ISO-10303-21;
HEADER;
/* Generated by software containing ST-Developer
 * from STEP Tools, Inc. (www.steptools.com) 
 */

FILE_DESCRIPTION(
/* description */ ('Caster wheel assembly'),
/* implementation_level */ '2;1');

FILE_NAME(
/* name */ 'Flat Washer - M8.step',
/* time_stamp */ '2026-10-28T03:23:56-07:00',
/* author */ (''),
/* organization */ (''),
/* preprocessor_version */ 'ST-DEVELOPER v20.2',
/* originating_system */ 'Autodesk Translation Framework v15.17.0.0',
/* authorisation */ '');

FILE_SCHEMA (('AUTOMOTIVE_DESIGN { 1 0 10303 214 3 1 1 }'));
ENDSEC;

DATA;
#10=MECHANICAL_DESIGN_GEOMETRIC_PRESENTATION_REPRESENTATION('',(#225),#5385);
#181=SHAPE_REPRESENTATION_RELATIONSHIP('SRR','None',#5476,#203);
#203=ADVANCED_BREP_SHAPE_REPRESENTATION('',(#255),#5363);
#225=STYLED_ITEM('',(#5679),#255);
#255=MANIFOLD_SOLID_BREP('Body1',#2652);
#295=FACE_BOUND('',#628,.T.);
#296=FACE_BOUND('',#630,.T.);
#345=PLANE('',#2977);
#346=PLANE('',#2978);
#443=FACE_OUTER_BOUND('',#625,.T.);
#444=FACE_OUTER_BOUND('',#626,.T.);
#445=FACE_OUTER_BOUND('',#627,.T.);
#446=FACE_OUTER_BOUND('',#629,.T.);
#625=EDGE_LOOP('',(#1866,#1867,#1868,#1869));
#626=EDGE_LOOP('',(#1870,#1871,#1872,#1873));
#627=EDGE_LOOP('',(#1874));
#628=EDGE_LOOP('',(#1875));
#629=EDGE_LOOP('',(#1876));
#630=EDGE_LOOP('',(#1877));
#831=LINE('',#4302,#965);
#832=LINE('',#4308,#966);
#965=VECTOR('',#3426,0.42);
#966=VECTOR('',#3433,0.8);
#1097=CIRCLE('',#2972,0.42);
#1098=CIRCLE('',#2973,0.42);
#1099=CIRCLE('',#2975,0.8);
#1100=CIRCLE('',#2976,0.8);
#1264=VERTEX_POINT('',#4299);
#1265=VERTEX_POINT('',#4301);
#1266=VERTEX_POINT('',#4305);
#1267=VERTEX_POINT('',#4307);
#1501=EDGE_CURVE('',#1264,#1264,#1097,.T.);
#1502=EDGE_CURVE('',#1264,#1265,#831,.T.);
#1503=EDGE_CURVE('',#1265,#1265,#1098,.T.);
#1504=EDGE_CURVE('',#1266,#1266,#1099,.T.);
#1505=EDGE_CURVE('',#1266,#1267,#832,.T.);
#1506=EDGE_CURVE('',#1267,#1267,#1100,.T.);
#1866=ORIENTED_EDGE('',*,*,#1501,.F.);
#1867=ORIENTED_EDGE('',*,*,#1502,.T.);
#1868=ORIENTED_EDGE('',*,*,#1503,.T.);
#1869=ORIENTED_EDGE('',*,*,#1502,.F.);
#1870=ORIENTED_EDGE('',*,*,#1504,.F.);
#1871=ORIENTED_EDGE('',*,*,#1505,.T.);
#1872=ORIENTED_EDGE('',*,*,#1506,.T.);
#1873=ORIENTED_EDGE('',*,*,#1505,.F.);
#1874=ORIENTED_EDGE('',*,*,#1504,.T.);
#1875=ORIENTED_EDGE('',*,*,#1501,.T.);
#1876=ORIENTED_EDGE('',*,*,#1506,.F.);
#1877=ORIENTED_EDGE('',*,*,#1503,.F.);
#2438=CYLINDRICAL_SURFACE('',#2971,0.42);
#2439=CYLINDRICAL_SURFACE('',#2974,0.8);
#2503=ADVANCED_FACE('',(#443),#2438,.F.);
#2504=ADVANCED_FACE('',(#444),#2439,.T.);
#2505=ADVANCED_FACE('',(#445,#295),#345,.T.);
#2506=ADVANCED_FACE('',(#446,#296),#346,.F.);
#2652=CLOSED_SHELL('',(#2503,#2504,#2505,#2506));
#2970=AXIS2_PLACEMENT_3D('',#4297,#3420,#3421);
#2971=AXIS2_PLACEMENT_3D('',#4298,#3422,#3423);
#2972=AXIS2_PLACEMENT_3D('',#4300,#3424,#3425);
#2973=AXIS2_PLACEMENT_3D('',#4303,#3427,#3428);
#2974=AXIS2_PLACEMENT_3D('',#4304,#3429,#3430);
#2975=AXIS2_PLACEMENT_3D('',#4306,#3431,#3432);
#2976=AXIS2_PLACEMENT_3D('',#4309,#3434,#3435);
#2977=AXIS2_PLACEMENT_3D('',#4310,#3436,#3437);
#2978=AXIS2_PLACEMENT_3D('',#4311,#3438,#3439);
#3420=DIRECTION('axis',(0.,0.,1.));
#3421=DIRECTION('refdir',(1.,0.,0.));
#3422=DIRECTION('center_axis',(0.,1.,0.));
#3423=DIRECTION('ref_axis',(1.,0.,0.));
#3424=DIRECTION('center_axis',(0.,-1.,0.));
#3425=DIRECTION('ref_axis',(1.,0.,0.));
#3426=DIRECTION('',(0.,-1.,0.));
#3427=DIRECTION('center_axis',(0.,-1.,0.));
#3428=DIRECTION('ref_axis',(1.,0.,0.));
#3429=DIRECTION('center_axis',(0.,1.,0.));
#3430=DIRECTION('ref_axis',(1.,0.,0.));
#3431=DIRECTION('center_axis',(0.,1.,0.));
#3432=DIRECTION('ref_axis',(1.,0.,0.));
#3433=DIRECTION('',(0.,-1.,0.));
#3434=DIRECTION('center_axis',(0.,1.,0.));
#3435=DIRECTION('ref_axis',(1.,0.,0.));
#3436=DIRECTION('center_axis',(0.,1.,0.));
#3437=DIRECTION('ref_axis',(1.,0.,0.));
#3438=DIRECTION('center_axis',(0.,1.,0.));
#3439=DIRECTION('ref_axis',(1.,0.,0.));
#4297=CARTESIAN_POINT('',(0.,0.,0.));
#4298=CARTESIAN_POINT('Origin',(0.,0.,0.));
#4299=CARTESIAN_POINT('',(-0.42,0.16,5.14351655641888E-17));
#4300=CARTESIAN_POINT('Origin',(0.,0.16,0.));
#4301=CARTESIAN_POINT('',(-0.42,0.,5.14351655641888E-17));
#4302=CARTESIAN_POINT('',(-0.42,0.,5.14351655641888E-17));
#4303=CARTESIAN_POINT('Origin',(0.,0.,0.));
#4304=CARTESIAN_POINT('Origin',(0.,0.,0.));
#4305=CARTESIAN_POINT('',(-0.8,0.16,9.79717439317883E-17));
#4306=CARTESIAN_POINT('Origin',(0.,0.16,0.));
#4307=CARTESIAN_POINT('',(-0.8,0.,9.79717439317883E-17));
#4308=CARTESIAN_POINT('',(-0.8,0.,9.79717439317883E-17));
#4309=CARTESIAN_POINT('Origin',(0.,0.,0.));
#4310=CARTESIAN_POINT('Origin',(0.,0.16,0.));
#4311=CARTESIAN_POINT('Origin',(0.,0.,0.));
#5335=UNCERTAINTY_MEASURE_WITH_UNIT(LENGTH_MEASURE(0.001),#5386,
'DISTANCE_ACCURACY_VALUE',
'Maximum model space distance between geometric entities at asserted c
onnectivities');
#5357=UNCERTAINTY_MEASURE_WITH_UNIT(LENGTH_MEASURE(0.001),#5386,
'DISTANCE_ACCURACY_VALUE',
'Maximum model space distance between geometric entities at asserted c
onnectivities');
#5363=(
GEOMETRIC_REPRESENTATION_CONTEXT(3)
GLOBAL_UNCERTAINTY_ASSIGNED_CONTEXT((#5335))
GLOBAL_UNIT_ASSIGNED_CONTEXT((#5386,#5388,#5389))
REPRESENTATION_CONTEXT('','3D')
);
#5385=(
GEOMETRIC_REPRESENTATION_CONTEXT(3)
GLOBAL_UNCERTAINTY_ASSIGNED_CONTEXT((#5357))
GLOBAL_UNIT_ASSIGNED_CONTEXT((#5386,#5388,#5389))
REPRESENTATION_CONTEXT('','3D')
);
#5386=(
LENGTH_UNIT()
NAMED_UNIT(*)
SI_UNIT(.CENTI.,.METRE.)
);
#5388=(
NAMED_UNIT(*)
PLANE_ANGLE_UNIT()
SI_UNIT($,.RADIAN.)
);
#5389=(
NAMED_UNIT(*)
SI_UNIT($,.STERADIAN.)
SOLID_ANGLE_UNIT()
);
#5395=SHAPE_DEFINITION_REPRESENTATION(#5422,#5476);
#5422=PRODUCT_DEFINITION_SHAPE('',$,#5504);
#5476=SHAPE_REPRESENTATION('',(#2970),#5363);
#5498=PRODUCT_DEFINITION_CONTEXT('part definition',#5581,'design');
#5504=PRODUCT_DEFINITION('Flat Washer - M8','Flat Washer - M8',#5531,#5498);
#5531=PRODUCT_DEFINITION_FORMATION('',$,#5588);
#5581=APPLICATION_CONTEXT(
'Core Data for Automotive Mechanical Design Process');
#5582=PRODUCT_CONTEXT('part definition',#5581,'mechanical');
#5588=PRODUCT('Flat Washer - M8','Flat Washer - M8','Flat Washer - M8',
(#5582));
#5673=COLOUR_RGB('Black',0.12,0.14,0.17);
#5674=FILL_AREA_STYLE_COLOUR('',#5673);
#5675=FILL_AREA_STYLE('',(#5674));
#5676=SURFACE_STYLE_FILL_AREA(#5675);
#5677=SURFACE_SIDE_STYLE('',(#5676));
#5678=SURFACE_STYLE_USAGE(.BOTH.,#5677);
#5679=PRESENTATION_STYLE_ASSIGNMENT((#5678));
ENDSEC;
END-ISO-10303-21;
